ISO-10303-21;
HEADER;
/* Generated by software containing ST-Developer
 * from STEP Tools, Inc. (www.steptools.com) 
 */

FILE_DESCRIPTION(
/* description */ ('Counterbalanced vertical column'),
/* implementation_level */ '2;1');

FILE_NAME(
/* name */ 'M5x14 Cap Screw.step',
/* time_stamp */ '2026-10-29T16:47:22-07:00',
/* author */ (''),
/* organization */ (''),
/* preprocessor_version */ 'ST-DEVELOPER v20.2',
/* originating_system */ 'Autodesk Translation Framework v15.17.0.0',
/* authorisation */ '');

FILE_SCHEMA (('AUTOMOTIVE_DESIGN { 1 0 10303 214 3 1 1 }'));
ENDSEC;

DATA;
#10=MECHANICAL_DESIGN_GEOMETRIC_PRESENTATION_REPRESENTATION('',(#383),#15040);
#255=CONICAL_SURFACE('',#8128,0.4,0.785398163397448);
#256=CONICAL_SURFACE('',#8132,0.41,0.785398163397448);
#257=CONICAL_SURFACE('',#8136,0.26,0.463647609000806);
#264=ORIENTED_CLOSED_SHELL('',*,#7108,.F.);
#268=BREP_WITH_VOIDS('Body1',#7109,(#264));
#313=SHAPE_REPRESENTATION_RELATIONSHIP('SRR','None',#15219,#348);
#348=ADVANCED_BREP_SHAPE_REPRESENTATION('',(#268),#15038);
#383=STYLED_ITEM('',(#15464),#268);
#529=FACE_BOUND('',#1730,.T.);
#804=PLANE('',#8116);
#805=PLANE('',#8117);
#806=PLANE('',#8118);
#807=PLANE('',#8119);
#808=PLANE('',#8120);
#809=PLANE('',#8121);
#810=PLANE('',#8122);
#811=PLANE('',#8123);
#812=PLANE('',#8124);
#813=PLANE('',#8126);
#814=PLANE('',#8134);
#1198=FACE_OUTER_BOUND('',#1716,.T.);
#1199=FACE_OUTER_BOUND('',#1717,.T.);
#1200=FACE_OUTER_BOUND('',#1718,.T.);
#1201=FACE_OUTER_BOUND('',#1719,.T.);
#1202=FACE_OUTER_BOUND('',#1720,.T.);
#1203=FACE_OUTER_BOUND('',#1721,.T.);
#1204=FACE_OUTER_BOUND('',#1722,.T.);
#1205=FACE_OUTER_BOUND('',#1723,.T.);
#1206=FACE_OUTER_BOUND('',#1724,.T.);
#1207=FACE_OUTER_BOUND('',#1725,.T.);
#1208=FACE_OUTER_BOUND('',#1726,.T.);
#1209=FACE_OUTER_BOUND('',#1727,.T.);
#1210=FACE_OUTER_BOUND('',#1728,.T.);
#1211=FACE_OUTER_BOUND('',#1729,.T.);
#1212=FACE_OUTER_BOUND('',#1731,.T.);
#1213=FACE_OUTER_BOUND('',#1732,.T.);
#1716=EDGE_LOOP('',(#6450,#6451,#6452,#6453));
#1717=EDGE_LOOP('',(#6454,#6455,#6456,#6457));
#1718=EDGE_LOOP('',(#6458,#6459,#6460,#6461));
#1719=EDGE_LOOP('',(#6462,#6463,#6464,#6465));
#1720=EDGE_LOOP('',(#6466,#6467,#6468,#6469));
#1721=EDGE_LOOP('',(#6470,#6471,#6472,#6473));
#1722=EDGE_LOOP('',(#6474,#6475,#6476,#6477,#6478,#6479));
#1723=EDGE_LOOP('',(#6480,#6481,#6482,#6483,#6484,#6485));
#1724=EDGE_LOOP('',(#6486));
#1725=EDGE_LOOP('',(#6487));
#1726=EDGE_LOOP('',(#6488,#6489,#6490,#6491));
#1727=EDGE_LOOP('',(#6492,#6493,#6494,#6495));
#1728=EDGE_LOOP('',(#6496,#6497,#6498,#6499));
#1729=EDGE_LOOP('',(#6500));
#1730=EDGE_LOOP('',(#6501));
#1731=EDGE_LOOP('',(#6502,#6503,#6504,#6505));
#1732=EDGE_LOOP('',(#6506,#6507,#6508,#6509));
#2375=LINE('',#14773,#3046);
#2376=LINE('',#14775,#3047);
#2377=LINE('',#14777,#3048);
#2378=LINE('',#14778,#3049);
#2379=LINE('',#14781,#3050);
#2380=LINE('',#14783,#3051);
#2381=LINE('',#14784,#3052);
#2382=LINE('',#14787,#3053);
#2383=LINE('',#14789,#3054);
#2384=LINE('',#14790,#3055);
#2385=LINE('',#14793,#3056);
#2386=LINE('',#14795,#3057);
#2387=LINE('',#14796,#3058);
#2388=LINE('',#14799,#3059);
#2389=LINE('',#14801,#3060);
#2390=LINE('',#14802,#3061);
#2391=LINE('',#14804,#3062);
#2392=LINE('',#14805,#3063);
#2393=LINE('',#14817,#3064);
#2394=LINE('',#14821,#3065);
#2395=LINE('',#14825,#3066);
#2396=LINE('',#14832,#3067);
#2397=LINE('',#14834,#3068);
#3046=VECTOR('',#10083,1.);
#3047=VECTOR('',#10084,1.);
#3048=VECTOR('',#10085,1.);
#3049=VECTOR('',#10086,1.);
#3050=VECTOR('',#10089,1.);
#3051=VECTOR('',#10090,1.);
#3052=VECTOR('',#10091,1.);
#3053=VECTOR('',#10094,1.);
#3054=VECTOR('',#10095,1.);
#3055=VECTOR('',#10096,1.);
#3056=VECTOR('',#10099,1.);
#3057=VECTOR('',#10100,1.);
#3058=VECTOR('',#10101,1.);
#3059=VECTOR('',#10104,1.);
#3060=VECTOR('',#10105,1.);
#3061=VECTOR('',#10106,1.);
#3062=VECTOR('',#10109,1.);
#3063=VECTOR('',#10110,1.);
#3064=VECTOR('',#10127,0.4);
#3065=VECTOR('',#10132,0.425);
#3066=VECTOR('',#10137,0.41);
#3067=VECTOR('',#10146,0.26);
#3068=VECTOR('',#10149,0.25);
#3291=CIRCLE('',#8125,0.24505);
#3292=CIRCLE('',#8127,0.375);
#3293=CIRCLE('',#8129,0.425);
#3294=CIRCLE('',#8131,0.425);
#3295=CIRCLE('',#8133,0.395);
#3296=CIRCLE('',#8135,0.27);
#3297=CIRCLE('',#8137,0.24505);
#3856=VERTEX_POINT('',#14771);
#3857=VERTEX_POINT('',#14772);
#3858=VERTEX_POINT('',#14774);
#3859=VERTEX_POINT('',#14776);
#3860=VERTEX_POINT('',#14780);
#3861=VERTEX_POINT('',#14782);
#3862=VERTEX_POINT('',#14786);
#3863=VERTEX_POINT('',#14788);
#3864=VERTEX_POINT('',#14792);
#3865=VERTEX_POINT('',#14794);
#3866=VERTEX_POINT('',#14798);
#3867=VERTEX_POINT('',#14800);
#3868=VERTEX_POINT('',#14809);
#3869=VERTEX_POINT('',#14812);
#3870=VERTEX_POINT('',#14815);
#3871=VERTEX_POINT('',#14819);
#3872=VERTEX_POINT('',#14823);
#3873=VERTEX_POINT('',#14827);
#3874=VERTEX_POINT('',#14830);
#4726=EDGE_CURVE('',#3856,#3857,#2375,.T.);
#4727=EDGE_CURVE('',#3857,#3858,#2376,.T.);
#4728=EDGE_CURVE('',#3858,#3859,#2377,.T.);
#4729=EDGE_CURVE('',#3856,#3859,#2378,.T.);
#4730=EDGE_CURVE('',#3857,#3860,#2379,.T.);
#4731=EDGE_CURVE('',#3860,#3861,#2380,.T.);
#4732=EDGE_CURVE('',#3861,#3858,#2381,.T.);
#4733=EDGE_CURVE('',#3860,#3862,#2382,.T.);
#4734=EDGE_CURVE('',#3862,#3863,#2383,.T.);
#4735=EDGE_CURVE('',#3863,#3861,#2384,.T.);
#4736=EDGE_CURVE('',#3862,#3864,#2385,.T.);
#4737=EDGE_CURVE('',#3864,#3865,#2386,.T.);
#4738=EDGE_CURVE('',#3865,#3863,#2387,.T.);
#4739=EDGE_CURVE('',#3864,#3866,#2388,.T.);
#4740=EDGE_CURVE('',#3866,#3867,#2389,.T.);
#4741=EDGE_CURVE('',#3867,#3865,#2390,.T.);
#4742=EDGE_CURVE('',#3866,#3856,#2391,.T.);
#4743=EDGE_CURVE('',#3859,#3867,#2392,.T.);
#4744=EDGE_CURVE('',#3868,#3868,#3291,.T.);
#4745=EDGE_CURVE('',#3869,#3869,#3292,.T.);
#4746=EDGE_CURVE('',#3870,#3870,#3293,.T.);
#4747=EDGE_CURVE('',#3870,#3869,#2393,.T.);
#4748=EDGE_CURVE('',#3871,#3871,#3294,.T.);
#4749=EDGE_CURVE('',#3871,#3870,#2394,.T.);
#4750=EDGE_CURVE('',#3872,#3872,#3295,.T.);
#4751=EDGE_CURVE('',#3872,#3871,#2395,.T.);
#4752=EDGE_CURVE('',#3873,#3873,#3296,.T.);
#4753=EDGE_CURVE('',#3874,#3874,#3297,.F.);
#4754=EDGE_CURVE('',#3874,#3873,#2396,.T.);
#4755=EDGE_CURVE('',#3868,#3874,#2397,.T.);
#6450=ORIENTED_EDGE('',*,*,#4726,.T.);
#6451=ORIENTED_EDGE('',*,*,#4727,.T.);
#6452=ORIENTED_EDGE('',*,*,#4728,.T.);
#6453=ORIENTED_EDGE('',*,*,#4729,.F.);
#6454=ORIENTED_EDGE('',*,*,#4730,.T.);
#6455=ORIENTED_EDGE('',*,*,#4731,.T.);
#6456=ORIENTED_EDGE('',*,*,#4732,.T.);
#6457=ORIENTED_EDGE('',*,*,#4727,.F.);
#6458=ORIENTED_EDGE('',*,*,#4733,.T.);
#6459=ORIENTED_EDGE('',*,*,#4734,.T.);
#6460=ORIENTED_EDGE('',*,*,#4735,.T.);
#6461=ORIENTED_EDGE('',*,*,#4731,.F.);
#6462=ORIENTED_EDGE('',*,*,#4736,.T.);
#6463=ORIENTED_EDGE('',*,*,#4737,.T.);
#6464=ORIENTED_EDGE('',*,*,#4738,.T.);
#6465=ORIENTED_EDGE('',*,*,#4734,.F.);
#6466=ORIENTED_EDGE('',*,*,#4739,.T.);
#6467=ORIENTED_EDGE('',*,*,#4740,.T.);
#6468=ORIENTED_EDGE('',*,*,#4741,.T.);
#6469=ORIENTED_EDGE('',*,*,#4737,.F.);
#6470=ORIENTED_EDGE('',*,*,#4742,.T.);
#6471=ORIENTED_EDGE('',*,*,#4729,.T.);
#6472=ORIENTED_EDGE('',*,*,#4743,.T.);
#6473=ORIENTED_EDGE('',*,*,#4740,.F.);
#6474=ORIENTED_EDGE('',*,*,#4742,.F.);
#6475=ORIENTED_EDGE('',*,*,#4739,.F.);
#6476=ORIENTED_EDGE('',*,*,#4736,.F.);
#6477=ORIENTED_EDGE('',*,*,#4733,.F.);
#6478=ORIENTED_EDGE('',*,*,#4730,.F.);
#6479=ORIENTED_EDGE('',*,*,#4726,.F.);
#6480=ORIENTED_EDGE('',*,*,#4743,.F.);
#6481=ORIENTED_EDGE('',*,*,#4728,.F.);
#6482=ORIENTED_EDGE('',*,*,#4732,.F.);
#6483=ORIENTED_EDGE('',*,*,#4735,.F.);
#6484=ORIENTED_EDGE('',*,*,#4738,.F.);
#6485=ORIENTED_EDGE('',*,*,#4741,.F.);
#6486=ORIENTED_EDGE('',*,*,#4744,.F.);
#6487=ORIENTED_EDGE('',*,*,#4745,.F.);
#6488=ORIENTED_EDGE('',*,*,#4746,.F.);
#6489=ORIENTED_EDGE('',*,*,#4747,.T.);
#6490=ORIENTED_EDGE('',*,*,#4745,.T.);
#6491=ORIENTED_EDGE('',*,*,#4747,.F.);
#6492=ORIENTED_EDGE('',*,*,#4748,.F.);
#6493=ORIENTED_EDGE('',*,*,#4749,.T.);
#6494=ORIENTED_EDGE('',*,*,#4746,.T.);
#6495=ORIENTED_EDGE('',*,*,#4749,.F.);
#6496=ORIENTED_EDGE('',*,*,#4750,.F.);
#6497=ORIENTED_EDGE('',*,*,#4751,.T.);
#6498=ORIENTED_EDGE('',*,*,#4748,.T.);
#6499=ORIENTED_EDGE('',*,*,#4751,.F.);
#6500=ORIENTED_EDGE('',*,*,#4750,.T.);
#6501=ORIENTED_EDGE('',*,*,#4752,.F.);
#6502=ORIENTED_EDGE('',*,*,#4753,.F.);
#6503=ORIENTED_EDGE('',*,*,#4754,.T.);
#6504=ORIENTED_EDGE('',*,*,#4752,.T.);
#6505=ORIENTED_EDGE('',*,*,#4754,.F.);
#6506=ORIENTED_EDGE('',*,*,#4744,.T.);
#6507=ORIENTED_EDGE('',*,*,#4755,.T.);
#6508=ORIENTED_EDGE('',*,*,#4753,.T.);
#6509=ORIENTED_EDGE('',*,*,#4755,.F.);
#6664=CYLINDRICAL_SURFACE('',#8130,0.425);
#6665=CYLINDRICAL_SURFACE('',#8138,0.24505);
#7040=ADVANCED_FACE('',(#1198),#804,.F.);
#7041=ADVANCED_FACE('',(#1199),#805,.F.);
#7042=ADVANCED_FACE('',(#1200),#806,.F.);
#7043=ADVANCED_FACE('',(#1201),#807,.F.);
#7044=ADVANCED_FACE('',(#1202),#808,.F.);
#7045=ADVANCED_FACE('',(#1203),#809,.F.);
#7046=ADVANCED_FACE('',(#1204),#810,.F.);
#7047=ADVANCED_FACE('',(#1205),#811,.F.);
#7048=ADVANCED_FACE('',(#1206),#812,.F.);
#7049=ADVANCED_FACE('',(#1207),#813,.T.);
#7050=ADVANCED_FACE('',(#1208),#255,.T.);
#7051=ADVANCED_FACE('',(#1209),#6664,.T.);
#7052=ADVANCED_FACE('',(#1210),#256,.T.);
#7053=ADVANCED_FACE('',(#1211,#529),#814,.T.);
#7054=ADVANCED_FACE('',(#1212),#257,.T.);
#7055=ADVANCED_FACE('',(#1213),#6665,.T.);
#7108=CLOSED_SHELL('',(#7040,#7041,#7042,#7043,#7044,#7045,#7046,#7047));
#7109=CLOSED_SHELL('',(#7048,#7049,#7050,#7051,#7052,#7053,#7054,#7055));
#8115=AXIS2_PLACEMENT_3D('',#14769,#10079,#10080);
#8116=AXIS2_PLACEMENT_3D('',#14770,#10081,#10082);
#8117=AXIS2_PLACEMENT_3D('',#14779,#10087,#10088);
#8118=AXIS2_PLACEMENT_3D('',#14785,#10092,#10093);
#8119=AXIS2_PLACEMENT_3D('',#14791,#10097,#10098);
#8120=AXIS2_PLACEMENT_3D('',#14797,#10102,#10103);
#8121=AXIS2_PLACEMENT_3D('',#14803,#10107,#10108);
#8122=AXIS2_PLACEMENT_3D('',#14806,#10111,#10112);
#8123=AXIS2_PLACEMENT_3D('',#14807,#10113,#10114);
#8124=AXIS2_PLACEMENT_3D('',#14808,#10115,#10116);
#8125=AXIS2_PLACEMENT_3D('',#14810,#10117,#10118);
#8126=AXIS2_PLACEMENT_3D('',#14811,#10119,#10120);
#8127=AXIS2_PLACEMENT_3D('',#14813,#10121,#10122);
#8128=AXIS2_PLACEMENT_3D('',#14814,#10123,#10124);
#8129=AXIS2_PLACEMENT_3D('',#14816,#10125,#10126);
#8130=AXIS2_PLACEMENT_3D('',#14818,#10128,#10129);
#8131=AXIS2_PLACEMENT_3D('',#14820,#10130,#10131);
#8132=AXIS2_PLACEMENT_3D('',#14822,#10133,#10134);
#8133=AXIS2_PLACEMENT_3D('',#14824,#10135,#10136);
#8134=AXIS2_PLACEMENT_3D('',#14826,#10138,#10139);
#8135=AXIS2_PLACEMENT_3D('',#14828,#10140,#10141);
#8136=AXIS2_PLACEMENT_3D('',#14829,#10142,#10143);
#8137=AXIS2_PLACEMENT_3D('',#14831,#10144,#10145);
#8138=AXIS2_PLACEMENT_3D('',#14833,#10147,#10148);
#10079=DIRECTION('axis',(0.,0.,1.));
#10080=DIRECTION('refdir',(1.,0.,0.));
#10081=DIRECTION('center_axis',(0.866025403784439,0.,-0.5));
#10082=DIRECTION('ref_axis',(0.5,0.,0.866025403784439));
#10083=DIRECTION('',(-0.5,0.,-0.866025403784439));
#10084=DIRECTION('',(0.,-1.,0.));
#10085=DIRECTION('',(0.5,0.,0.866025403784439));
#10086=DIRECTION('',(0.,-1.,0.));
#10087=DIRECTION('center_axis',(1.20185167898973E-16,0.,-1.));
#10088=DIRECTION('ref_axis',(1.,0.,1.20185167898973E-16));
#10089=DIRECTION('',(-1.,0.,-1.20185167898973E-16));
#10090=DIRECTION('',(0.,-1.,0.));
#10091=DIRECTION('',(1.,0.,1.20185167898973E-16));
#10092=DIRECTION('center_axis',(-0.866025403784439,0.,-0.5));
#10093=DIRECTION('ref_axis',(0.5,0.,-0.866025403784439));
#10094=DIRECTION('',(-0.5,0.,0.866025403784439));
#10095=DIRECTION('',(0.,-1.,0.));
#10096=DIRECTION('',(0.5,0.,-0.866025403784439));
#10097=DIRECTION('center_axis',(-0.866025403784439,0.,0.5));
#10098=DIRECTION('ref_axis',(-0.5,0.,-0.866025403784439));
#10099=DIRECTION('',(0.5,0.,0.866025403784439));
#10100=DIRECTION('',(0.,-1.,0.));
#10101=DIRECTION('',(-0.5,0.,-0.866025403784439));
#10102=DIRECTION('center_axis',(-2.40370335797945E-16,0.,1.));
#10103=DIRECTION('ref_axis',(-1.,0.,-2.40370335797945E-16));
#10104=DIRECTION('',(1.,0.,2.40370335797945E-16));
#10105=DIRECTION('',(0.,-1.,0.));
#10106=DIRECTION('',(-1.,0.,-2.40370335797945E-16));
#10107=DIRECTION('center_axis',(0.866025403784439,0.,0.5));
#10108=DIRECTION('ref_axis',(-0.5,0.,0.866025403784439));
#10109=DIRECTION('',(0.5,0.,-0.866025403784439));
#10110=DIRECTION('',(-0.5,0.,0.866025403784439));
#10111=DIRECTION('center_axis',(0.,1.,0.));
#10112=DIRECTION('ref_axis',(1.,0.,0.));
#10113=DIRECTION('center_axis',(0.,-1.,0.));
#10114=DIRECTION('ref_axis',(0.,0.,-1.));
#10115=DIRECTION('center_axis',(0.,1.,0.));
#10116=DIRECTION('ref_axis',(1.,0.,0.));
#10117=DIRECTION('center_axis',(0.,1.,0.));
#10118=DIRECTION('ref_axis',(1.,0.,0.));
#10119=DIRECTION('center_axis',(0.,1.,0.));
#10120=DIRECTION('ref_axis',(0.,0.,1.));
#10121=DIRECTION('center_axis',(0.,-1.,0.));
#10122=DIRECTION('ref_axis',(1.,0.,0.));
#10123=DIRECTION('center_axis',(0.,-1.,0.));
#10124=DIRECTION('ref_axis',(1.,0.,0.));
#10125=DIRECTION('center_axis',(0.,-1.,0.));
#10126=DIRECTION('ref_axis',(1.,0.,0.));
#10127=DIRECTION('',(0.707106781186548,0.707106781186547,8.65956056235493E-17));
#10128=DIRECTION('center_axis',(0.,-1.,0.));
#10129=DIRECTION('ref_axis',(1.,0.,0.));
#10130=DIRECTION('center_axis',(0.,-1.,0.));
#10131=DIRECTION('ref_axis',(1.,0.,0.));
#10132=DIRECTION('',(0.,1.,0.));
#10133=DIRECTION('center_axis',(0.,1.,0.));
#10134=DIRECTION('ref_axis',(1.,0.,0.));
#10135=DIRECTION('center_axis',(0.,-1.,0.));
#10136=DIRECTION('ref_axis',(1.,0.,0.));
#10137=DIRECTION('',(-0.707106781186547,0.707106781186548,-8.65956056235493E-17));
#10138=DIRECTION('center_axis',(0.,-1.,0.));
#10139=DIRECTION('ref_axis',(0.,0.,-1.));
#10140=DIRECTION('center_axis',(0.,-1.,0.));
#10141=DIRECTION('ref_axis',(1.,0.,0.));
#10142=DIRECTION('center_axis',(0.,1.,0.));
#10143=DIRECTION('ref_axis',(1.,0.,0.));
#10144=DIRECTION('center_axis',(0.,1.,0.));
#10145=DIRECTION('ref_axis',(1.,0.,0.));
#10146=DIRECTION('',(-0.447213595499958,0.894427190999916,-5.47678698264203E-17));
#10147=DIRECTION('center_axis',(0.,-1.,0.));
#10148=DIRECTION('ref_axis',(1.,0.,0.));
#10149=DIRECTION('',(0.,1.,0.));
#14769=CARTESIAN_POINT('',(0.,0.,0.));
#14770=CARTESIAN_POINT('Origin',(0.115470053837925,-0.5,-0.2));
#14771=CARTESIAN_POINT('',(0.23094010767585,-0.5,0.));
#14772=CARTESIAN_POINT('',(0.115470053837925,-0.5,-0.2));
#14773=CARTESIAN_POINT('',(0.23094010767585,-0.5,0.));
#14774=CARTESIAN_POINT('',(0.115470053837925,-0.8,-0.2));
#14775=CARTESIAN_POINT('',(0.115470053837925,-0.5,-0.2));
#14776=CARTESIAN_POINT('',(0.23094010767585,-0.8,0.));
#14777=CARTESIAN_POINT('',(0.23094010767585,-0.8,0.));
#14778=CARTESIAN_POINT('',(0.23094010767585,-0.5,0.));
#14779=CARTESIAN_POINT('Origin',(-0.115470053837925,-0.5,-0.2));
#14780=CARTESIAN_POINT('',(-0.115470053837925,-0.5,-0.2));
#14781=CARTESIAN_POINT('',(0.115470053837925,-0.5,-0.2));
#14782=CARTESIAN_POINT('',(-0.115470053837925,-0.8,-0.2));
#14783=CARTESIAN_POINT('',(-0.115470053837925,-0.5,-0.2));
#14784=CARTESIAN_POINT('',(0.115470053837925,-0.8,-0.2));
#14785=CARTESIAN_POINT('Origin',(-0.23094010767585,-0.5,-2.77555756156289E-17));
#14786=CARTESIAN_POINT('',(-0.23094010767585,-0.5,-2.82820063659975E-17));
#14787=CARTESIAN_POINT('',(-0.115470053837925,-0.5,-0.2));
#14788=CARTESIAN_POINT('',(-0.23094010767585,-0.8,-2.77555756156289E-17));
#14789=CARTESIAN_POINT('',(-0.23094010767585,-0.5,-2.82820063659975E-17));
#14790=CARTESIAN_POINT('',(-0.115470053837925,-0.8,-0.2));
#14791=CARTESIAN_POINT('Origin',(-0.115470053837925,-0.5,0.2));
#14792=CARTESIAN_POINT('',(-0.115470053837925,-0.5,0.2));
#14793=CARTESIAN_POINT('',(-0.23094010767585,-0.5,-2.82820063659975E-17));
#14794=CARTESIAN_POINT('',(-0.115470053837925,-0.8,0.2));
#14795=CARTESIAN_POINT('',(-0.115470053837925,-0.5,0.2));
#14796=CARTESIAN_POINT('',(-0.23094010767585,-0.8,-2.82820063659975E-17));
#14797=CARTESIAN_POINT('Origin',(0.115470053837925,-0.5,0.2));
#14798=CARTESIAN_POINT('',(0.115470053837925,-0.5,0.2));
#14799=CARTESIAN_POINT('',(-0.115470053837925,-0.5,0.2));
#14800=CARTESIAN_POINT('',(0.115470053837925,-0.8,0.2));
#14801=CARTESIAN_POINT('',(0.115470053837925,-0.5,0.2));
#14802=CARTESIAN_POINT('',(-0.115470053837925,-0.8,0.2));
#14803=CARTESIAN_POINT('Origin',(0.23094010767585,-0.5,0.));
#14804=CARTESIAN_POINT('',(0.115470053837925,-0.5,0.2));
#14805=CARTESIAN_POINT('',(0.115470053837925,-0.8,0.2));
#14806=CARTESIAN_POINT('Origin',(0.,-0.5,0.));
#14807=CARTESIAN_POINT('Origin',(0.,-0.8,0.));
#14808=CARTESIAN_POINT('Origin',(0.,-1.4,0.));
#14809=CARTESIAN_POINT('',(-0.24505,-1.4,3.00099698131059E-17));
#14810=CARTESIAN_POINT('Origin',(0.,-1.4,0.));
#14811=CARTESIAN_POINT('Origin',(0.375,0.5,0.));
#14812=CARTESIAN_POINT('',(-0.375,0.5,-4.59242549680257E-17));
#14813=CARTESIAN_POINT('Origin',(0.,0.5,0.));
#14814=CARTESIAN_POINT('Origin',(0.,0.475,0.));
#14815=CARTESIAN_POINT('',(-0.425,0.45,-5.20474889637625E-17));
#14816=CARTESIAN_POINT('Origin',(0.,0.45,0.));
#14817=CARTESIAN_POINT('',(-0.4,0.475,-4.89858719658941E-17));
#14818=CARTESIAN_POINT('Origin',(0.,0.24,0.));
#14819=CARTESIAN_POINT('',(-0.425,0.0299999999999998,-5.20474889637625E-17));
#14820=CARTESIAN_POINT('Origin',(0.,0.0299999999999998,0.));
#14821=CARTESIAN_POINT('',(-0.425,0.24,-5.20474889637625E-17));
#14822=CARTESIAN_POINT('Origin',(0.,0.0150000000000001,0.));
#14823=CARTESIAN_POINT('',(-0.395,4.85722573273506E-17,-4.83735485663204E-17));
#14824=CARTESIAN_POINT('Origin',(0.,0.,0.));
#14825=CARTESIAN_POINT('',(-0.41,0.0150000000000001,-5.02105187650415E-17));
#14826=CARTESIAN_POINT('Origin',(0.27,0.,0.));
#14827=CARTESIAN_POINT('',(-0.27,0.,-3.30654635769785E-17));
#14828=CARTESIAN_POINT('Origin',(0.,0.,0.));
#14829=CARTESIAN_POINT('Origin',(0.,-0.02,0.));
#14830=CARTESIAN_POINT('',(-0.24505,-0.0498999999999999,3.00099698131059E-17));
#14831=CARTESIAN_POINT('Origin',(0.,-0.0498999999999999,0.));
#14832=CARTESIAN_POINT('',(-0.26,-0.02,-3.18408167778312E-17));
#14833=CARTESIAN_POINT('Origin',(0.,-0.995,0.));
#14834=CARTESIAN_POINT('',(-0.24505,-0.995,-3.00099698131059E-17));
#14998=UNCERTAINTY_MEASURE_WITH_UNIT(LENGTH_MEASURE(0.001),#15041,
'DISTANCE_ACCURACY_VALUE',
'Maximum model space distance between geometric entities at asserted c
onnectivities');
#15000=UNCERTAINTY_MEASURE_WITH_UNIT(LENGTH_MEASURE(0.001),#15041,
'DISTANCE_ACCURACY_VALUE',
'Maximum model space distance between geometric entities at asserted c
onnectivities');
#15038=(
GEOMETRIC_REPRESENTATION_CONTEXT(3)
GLOBAL_UNCERTAINTY_ASSIGNED_CONTEXT((#14998))
GLOBAL_UNIT_ASSIGNED_CONTEXT((#15041,#15043,#15044))
REPRESENTATION_CONTEXT('','3D')
);
#15040=(
GEOMETRIC_REPRESENTATION_CONTEXT(3)
GLOBAL_UNCERTAINTY_ASSIGNED_CONTEXT((#15000))
GLOBAL_UNIT_ASSIGNED_CONTEXT((#15041,#15043,#15044))
REPRESENTATION_CONTEXT('','3D')
);
#15041=(
LENGTH_UNIT()
NAMED_UNIT(*)
SI_UNIT(.CENTI.,.METRE.)
);
#15043=(
NAMED_UNIT(*)
PLANE_ANGLE_UNIT()
SI_UNIT($,.RADIAN.)
);
#15044=(
NAMED_UNIT(*)
SI_UNIT($,.STERADIAN.)
SOLID_ANGLE_UNIT()
);
#15082=SHAPE_DEFINITION_REPRESENTATION(#15124,#15219);
#15124=PRODUCT_DEFINITION_SHAPE('',$,#15259);
#15219=SHAPE_REPRESENTATION('',(#8115),#15038);
#15221=PRODUCT_DEFINITION_CONTEXT('part definition',#15340,'design');
#15259=PRODUCT_DEFINITION('M5x14 Cap Screw','M5x14 Cap Screw',#15298,#15221);
#15298=PRODUCT_DEFINITION_FORMATION('',$,#15379);
#15340=APPLICATION_CONTEXT(
'Core Data for Automotive Mechanical Design Process');
#15341=PRODUCT_CONTEXT('part definition',#15340,'mechanical');
#15379=PRODUCT('M5x14 Cap Screw','M5x14 Cap Screw','M5x14 Cap Screw',(#15341));
#15458=COLOUR_RGB('Black',0.12,0.14,0.17);
#15459=FILL_AREA_STYLE_COLOUR('',#15458);
#15460=FILL_AREA_STYLE('',(#15459));
#15461=SURFACE_STYLE_FILL_AREA(#15460);
#15462=SURFACE_SIDE_STYLE('',(#15461));
#15463=SURFACE_STYLE_USAGE(.BOTH.,#15462);
#15464=PRESENTATION_STYLE_ASSIGNMENT((#15463));
ENDSEC;
END-ISO-10303-21;
